ISO-10303-21;
HEADER;
/* Generated by software containing ST-Developer
 * from STEP Tools, Inc. (www.steptools.com) 
 */

FILE_DESCRIPTION(
/* description */ (''),
/* implementation_level */ '2;1');

FILE_NAME(
/* name */ 'Ball_Screw_01.step',
/* time_stamp */ '2026-10-23T17:00:58+06:00',
/* author */ (''),
/* organization */ (''),
/* preprocessor_version */ 'ST-DEVELOPER v20.2',
/* originating_system */ 'Autodesk Translation Framework v15.15.0.0',
/* authorisation */ '');

FILE_SCHEMA (('AUTOMOTIVE_DESIGN { 1 0 10303 214 3 1 1 }'));
ENDSEC;

DATA;
#10=MECHANICAL_DESIGN_GEOMETRIC_PRESENTATION_REPRESENTATION('',(#109),#11385);
#63=SPHERICAL_SURFACE('',#5797,3.);
#74=TOROIDAL_SURFACE('',#5800,2.65761552865316,0.5);
#83=SHAPE_REPRESENTATION_RELATIONSHIP('SRR','None',#11435,#96);
#96=ADVANCED_BREP_SHAPE_REPRESENTATION('',(#122),#11375);
#109=STYLED_ITEM('',(#11574),#122);
#122=MANIFOLD_SOLID_BREP('Ball_Screw_01',#5345);
#151=FACE_BOUND('',#1114,.T.);
#152=FACE_BOUND('',#1124,.T.);
#226=CONICAL_SURFACE('',#5814,2.90761552865316,0.785398163397448);
#406=CIRCLE('',#5798,2.59807621135332);
#407=CIRCLE('',#5799,3.);
#408=CIRCLE('',#5801,2.65761552865316);
#409=CIRCLE('',#5802,0.5);
#410=CIRCLE('',#5803,3.15761552865316);
#411=CIRCLE('',#5805,3.15761552865316);
#412=CIRCLE('',#5815,2.65761552865316);
#578=CYLINDRICAL_SURFACE('',#5804,3.15761552865316);
#765=FACE_OUTER_BOUND('',#1110,.T.);
#766=FACE_OUTER_BOUND('',#1111,.T.);
#767=FACE_OUTER_BOUND('',#1112,.T.);
#768=FACE_OUTER_BOUND('',#1113,.T.);
#769=FACE_OUTER_BOUND('',#1115,.T.);
#770=FACE_OUTER_BOUND('',#1116,.T.);
#771=FACE_OUTER_BOUND('',#1117,.T.);
#772=FACE_OUTER_BOUND('',#1118,.T.);
#773=FACE_OUTER_BOUND('',#1119,.T.);
#774=FACE_OUTER_BOUND('',#1120,.T.);
#775=FACE_OUTER_BOUND('',#1121,.T.);
#776=FACE_OUTER_BOUND('',#1122,.T.);
#777=FACE_OUTER_BOUND('',#1123,.T.);
#1110=EDGE_LOOP('',(#4160,#4161,#4162));
#1111=EDGE_LOOP('',(#4163,#4164,#4165,#4166));
#1112=EDGE_LOOP('',(#4167,#4168,#4169,#4170));
#1113=EDGE_LOOP('',(#4171));
#1114=EDGE_LOOP('',(#4172));
#1115=EDGE_LOOP('',(#4173,#4174,#4175,#4176));
#1116=EDGE_LOOP('',(#4177,#4178,#4179,#4180));
#1117=EDGE_LOOP('',(#4181,#4182,#4183,#4184));
#1118=EDGE_LOOP('',(#4185,#4186,#4187,#4188));
#1119=EDGE_LOOP('',(#4189,#4190,#4191,#4192));
#1120=EDGE_LOOP('',(#4193,#4194,#4195,#4196));
#1121=EDGE_LOOP('',(#4197,#4198,#4199,#4200,#4201,#4202));
#1122=EDGE_LOOP('',(#4203,#4204,#4205,#4206));
#1123=EDGE_LOOP('',(#4207));
#1124=EDGE_LOOP('',(#4208,#4209,#4210,#4211,#4212,#4213));
#1541=LINE('',#9123,#2003);
#1542=LINE('',#9129,#2004);
#1543=LINE('',#9131,#2005);
#1544=LINE('',#9133,#2006);
#1545=LINE('',#9134,#2007);
#1546=LINE('',#9137,#2008);
#1547=LINE('',#9139,#2009);
#1548=LINE('',#9140,#2010);
#1549=LINE('',#9143,#2011);
#1550=LINE('',#9145,#2012);
#1551=LINE('',#9146,#2013);
#1552=LINE('',#9149,#2014);
#1553=LINE('',#9151,#2015);
#1554=LINE('',#9152,#2016);
#1555=LINE('',#9155,#2017);
#1556=LINE('',#9157,#2018);
#1557=LINE('',#9158,#2019);
#1558=LINE('',#9160,#2020);
#1559=LINE('',#9161,#2021);
#1560=LINE('',#9166,#2022);
#2003=VECTOR('',#6966,3.15761552865316);
#2004=VECTOR('',#6973,10.);
#2005=VECTOR('',#6974,10.);
#2006=VECTOR('',#6975,10.);
#2007=VECTOR('',#6976,10.);
#2008=VECTOR('',#6979,10.);
#2009=VECTOR('',#6980,10.);
#2010=VECTOR('',#6981,10.);
#2011=VECTOR('',#6984,10.);
#2012=VECTOR('',#6985,10.);
#2013=VECTOR('',#6986,10.);
#2014=VECTOR('',#6989,10.);
#2015=VECTOR('',#6990,10.);
#2016=VECTOR('',#6991,10.);
#2017=VECTOR('',#6994,10.);
#2018=VECTOR('',#6995,10.);
#2019=VECTOR('',#6996,10.);
#2020=VECTOR('',#6999,10.);
#2021=VECTOR('',#7000,10.);
#2022=VECTOR('',#7007,2.90761552865316);
#2450=VERTEX_POINT('',#9111);
#2451=VERTEX_POINT('',#9113);
#2452=VERTEX_POINT('',#9116);
#2453=VERTEX_POINT('',#9118);
#2454=VERTEX_POINT('',#9122);
#2455=VERTEX_POINT('',#9127);
#2456=VERTEX_POINT('',#9128);
#2457=VERTEX_POINT('',#9130);
#2458=VERTEX_POINT('',#9132);
#2459=VERTEX_POINT('',#9136);
#2460=VERTEX_POINT('',#9138);
#2461=VERTEX_POINT('',#9142);
#2462=VERTEX_POINT('',#9144);
#2463=VERTEX_POINT('',#9148);
#2464=VERTEX_POINT('',#9150);
#2465=VERTEX_POINT('',#9154);
#2466=VERTEX_POINT('',#9156);
#2467=VERTEX_POINT('',#9164);
#3045=EDGE_CURVE('',#2450,#2450,#406,.T.);
#3046=EDGE_CURVE('',#2451,#2450,#407,.T.);
#3047=EDGE_CURVE('',#2452,#2452,#408,.T.);
#3048=EDGE_CURVE('',#2452,#2453,#409,.T.);
#3049=EDGE_CURVE('',#2453,#2453,#410,.T.);
#3050=EDGE_CURVE('',#2453,#2454,#1541,.T.);
#3051=EDGE_CURVE('',#2454,#2454,#411,.T.);
#3052=EDGE_CURVE('',#2455,#2456,#1542,.T.);
#3053=EDGE_CURVE('',#2455,#2457,#1543,.T.);
#3054=EDGE_CURVE('',#2457,#2458,#1544,.T.);
#3055=EDGE_CURVE('',#2456,#2458,#1545,.T.);
#3056=EDGE_CURVE('',#2459,#2455,#1546,.T.);
#3057=EDGE_CURVE('',#2459,#2460,#1547,.T.);
#3058=EDGE_CURVE('',#2460,#2457,#1548,.T.);
#3059=EDGE_CURVE('',#2461,#2459,#1549,.T.);
#3060=EDGE_CURVE('',#2461,#2462,#1550,.T.);
#3061=EDGE_CURVE('',#2462,#2460,#1551,.T.);
#3062=EDGE_CURVE('',#2463,#2461,#1552,.T.);
#3063=EDGE_CURVE('',#2463,#2464,#1553,.T.);
#3064=EDGE_CURVE('',#2464,#2462,#1554,.T.);
#3065=EDGE_CURVE('',#2465,#2463,#1555,.T.);
#3066=EDGE_CURVE('',#2465,#2466,#1556,.T.);
#3067=EDGE_CURVE('',#2466,#2464,#1557,.T.);
#3068=EDGE_CURVE('',#2456,#2465,#1558,.T.);
#3069=EDGE_CURVE('',#2458,#2466,#1559,.T.);
#3070=EDGE_CURVE('',#2467,#2467,#412,.T.);
#3071=EDGE_CURVE('',#2467,#2454,#1560,.T.);
#4160=ORIENTED_EDGE('',*,*,#3045,.F.);
#4161=ORIENTED_EDGE('',*,*,#3046,.F.);
#4162=ORIENTED_EDGE('',*,*,#3046,.T.);
#4163=ORIENTED_EDGE('',*,*,#3047,.T.);
#4164=ORIENTED_EDGE('',*,*,#3048,.T.);
#4165=ORIENTED_EDGE('',*,*,#3049,.T.);
#4166=ORIENTED_EDGE('',*,*,#3048,.F.);
#4167=ORIENTED_EDGE('',*,*,#3049,.F.);
#4168=ORIENTED_EDGE('',*,*,#3050,.T.);
#4169=ORIENTED_EDGE('',*,*,#3051,.F.);
#4170=ORIENTED_EDGE('',*,*,#3050,.F.);
#4171=ORIENTED_EDGE('',*,*,#3047,.F.);
#4172=ORIENTED_EDGE('',*,*,#3045,.T.);
#4173=ORIENTED_EDGE('',*,*,#3052,.F.);
#4174=ORIENTED_EDGE('',*,*,#3053,.T.);
#4175=ORIENTED_EDGE('',*,*,#3054,.T.);
#4176=ORIENTED_EDGE('',*,*,#3055,.F.);
#4177=ORIENTED_EDGE('',*,*,#3056,.F.);
#4178=ORIENTED_EDGE('',*,*,#3057,.T.);
#4179=ORIENTED_EDGE('',*,*,#3058,.T.);
#4180=ORIENTED_EDGE('',*,*,#3053,.F.);
#4181=ORIENTED_EDGE('',*,*,#3059,.F.);
#4182=ORIENTED_EDGE('',*,*,#3060,.T.);
#4183=ORIENTED_EDGE('',*,*,#3061,.T.);
#4184=ORIENTED_EDGE('',*,*,#3057,.F.);
#4185=ORIENTED_EDGE('',*,*,#3062,.F.);
#4186=ORIENTED_EDGE('',*,*,#3063,.T.);
#4187=ORIENTED_EDGE('',*,*,#3064,.T.);
#4188=ORIENTED_EDGE('',*,*,#3060,.F.);
#4189=ORIENTED_EDGE('',*,*,#3065,.F.);
#4190=ORIENTED_EDGE('',*,*,#3066,.T.);
#4191=ORIENTED_EDGE('',*,*,#3067,.T.);
#4192=ORIENTED_EDGE('',*,*,#3063,.F.);
#4193=ORIENTED_EDGE('',*,*,#3068,.F.);
#4194=ORIENTED_EDGE('',*,*,#3055,.T.);
#4195=ORIENTED_EDGE('',*,*,#3069,.T.);
#4196=ORIENTED_EDGE('',*,*,#3066,.F.);
#4197=ORIENTED_EDGE('',*,*,#3069,.F.);
#4198=ORIENTED_EDGE('',*,*,#3054,.F.);
#4199=ORIENTED_EDGE('',*,*,#3058,.F.);
#4200=ORIENTED_EDGE('',*,*,#3061,.F.);
#4201=ORIENTED_EDGE('',*,*,#3064,.F.);
#4202=ORIENTED_EDGE('',*,*,#3067,.F.);
#4203=ORIENTED_EDGE('',*,*,#3070,.T.);
#4204=ORIENTED_EDGE('',*,*,#3071,.T.);
#4205=ORIENTED_EDGE('',*,*,#3051,.T.);
#4206=ORIENTED_EDGE('',*,*,#3071,.F.);
#4207=ORIENTED_EDGE('',*,*,#3070,.F.);
#4208=ORIENTED_EDGE('',*,*,#3052,.T.);
#4209=ORIENTED_EDGE('',*,*,#3068,.T.);
#4210=ORIENTED_EDGE('',*,*,#3065,.T.);
#4211=ORIENTED_EDGE('',*,*,#3062,.T.);
#4212=ORIENTED_EDGE('',*,*,#3059,.T.);
#4213=ORIENTED_EDGE('',*,*,#3056,.T.);
#4939=PLANE('',#5806);
#4940=PLANE('',#5807);
#4941=PLANE('',#5808);
#4942=PLANE('',#5809);
#4943=PLANE('',#5810);
#4944=PLANE('',#5811);
#4945=PLANE('',#5812);
#4946=PLANE('',#5813);
#4947=PLANE('',#5816);
#5177=ADVANCED_FACE('',(#765),#63,.T.);
#5178=ADVANCED_FACE('',(#766),#74,.T.);
#5179=ADVANCED_FACE('',(#767),#578,.T.);
#5180=ADVANCED_FACE('',(#768,#151),#4939,.F.);
#5181=ADVANCED_FACE('',(#769),#4940,.F.);
#5182=ADVANCED_FACE('',(#770),#4941,.F.);
#5183=ADVANCED_FACE('',(#771),#4942,.F.);
#5184=ADVANCED_FACE('',(#772),#4943,.F.);
#5185=ADVANCED_FACE('',(#773),#4944,.F.);
#5186=ADVANCED_FACE('',(#774),#4945,.F.);
#5187=ADVANCED_FACE('',(#775),#4946,.F.);
#5188=ADVANCED_FACE('',(#776),#226,.T.);
#5189=ADVANCED_FACE('',(#777,#152),#4947,.T.);
#5345=CLOSED_SHELL('',(#5177,#5178,#5179,#5180,#5181,#5182,#5183,#5184,
#5185,#5186,#5187,#5188,#5189));
#5796=AXIS2_PLACEMENT_3D('',#9109,#6948,#6949);
#5797=AXIS2_PLACEMENT_3D('',#9110,#6950,#6951);
#5798=AXIS2_PLACEMENT_3D('',#9112,#6952,#6953);
#5799=AXIS2_PLACEMENT_3D('',#9114,#6954,#6955);
#5800=AXIS2_PLACEMENT_3D('',#9115,#6956,#6957);
#5801=AXIS2_PLACEMENT_3D('',#9117,#6958,#6959);
#5802=AXIS2_PLACEMENT_3D('',#9119,#6960,#6961);
#5803=AXIS2_PLACEMENT_3D('',#9120,#6962,#6963);
#5804=AXIS2_PLACEMENT_3D('',#9121,#6964,#6965);
#5805=AXIS2_PLACEMENT_3D('',#9124,#6967,#6968);
#5806=AXIS2_PLACEMENT_3D('',#9125,#6969,#6970);
#5807=AXIS2_PLACEMENT_3D('',#9126,#6971,#6972);
#5808=AXIS2_PLACEMENT_3D('',#9135,#6977,#6978);
#5809=AXIS2_PLACEMENT_3D('',#9141,#6982,#6983);
#5810=AXIS2_PLACEMENT_3D('',#9147,#6987,#6988);
#5811=AXIS2_PLACEMENT_3D('',#9153,#6992,#6993);
#5812=AXIS2_PLACEMENT_3D('',#9159,#6997,#6998);
#5813=AXIS2_PLACEMENT_3D('',#9162,#7001,#7002);
#5814=AXIS2_PLACEMENT_3D('',#9163,#7003,#7004);
#5815=AXIS2_PLACEMENT_3D('',#9165,#7005,#7006);
#5816=AXIS2_PLACEMENT_3D('',#9167,#7008,#7009);
#6948=DIRECTION('axis',(0.,0.,1.));
#6949=DIRECTION('refdir',(1.,0.,0.));
#6950=DIRECTION('center_axis',(0.,0.,-1.));
#6951=DIRECTION('ref_axis',(1.,0.,0.));
#6952=DIRECTION('center_axis',(0.,-1.22464679914735E-16,1.));
#6953=DIRECTION('ref_axis',(0.,-1.,-1.22464679914735E-16));
#6954=DIRECTION('center_axis',(0.,1.,1.22464679914735E-16));
#6955=DIRECTION('ref_axis',(-1.,0.,0.));
#6956=DIRECTION('center_axis',(0.,1.22464679914735E-16,-1.));
#6957=DIRECTION('ref_axis',(1.,0.,0.));
#6958=DIRECTION('center_axis',(0.,-1.22464679914735E-16,1.));
#6959=DIRECTION('ref_axis',(1.,0.,0.));
#6960=DIRECTION('center_axis',(0.,1.,1.22464679914735E-16));
#6961=DIRECTION('ref_axis',(-1.,0.,0.));
#6962=DIRECTION('center_axis',(0.,1.22464679914735E-16,-1.));
#6963=DIRECTION('ref_axis',(1.,0.,0.));
#6964=DIRECTION('center_axis',(0.,1.22464679914735E-16,-1.));
#6965=DIRECTION('ref_axis',(1.,0.,0.));
#6966=DIRECTION('',(0.,-1.22464679914735E-16,1.));
#6967=DIRECTION('center_axis',(0.,-1.22464679914735E-16,1.));
#6968=DIRECTION('ref_axis',(1.,0.,0.));
#6969=DIRECTION('center_axis',(0.,-1.22464679914735E-16,1.));
#6970=DIRECTION('ref_axis',(1.,0.,0.));
#6971=DIRECTION('center_axis',(-0.5,-0.866025403784439,-1.06057523872491E-16));
#6972=DIRECTION('ref_axis',(-0.866025403784439,0.5,6.12323399573677E-17));
#6973=DIRECTION('',(-0.866025403784439,0.5,6.12323399573677E-17));
#6974=DIRECTION('',(0.,1.22464679914735E-16,-1.));
#6975=DIRECTION('',(-0.866025403784439,0.5,6.12323399573677E-17));
#6976=DIRECTION('',(0.,1.22464679914735E-16,-1.));
#6977=DIRECTION('center_axis',(0.5,-0.866025403784439,-1.06057523872491E-16));
#6978=DIRECTION('ref_axis',(-0.866025403784439,-0.5,-6.12323399573677E-17));
#6979=DIRECTION('',(-0.866025403784439,-0.5,-6.12323399573677E-17));
#6980=DIRECTION('',(0.,1.22464679914735E-16,-1.));
#6981=DIRECTION('',(-0.866025403784439,-0.5,-6.12323399573677E-17));
#6982=DIRECTION('center_axis',(1.,0.,0.));
#6983=DIRECTION('ref_axis',(0.,-1.,-1.22464679914735E-16));
#6984=DIRECTION('',(0.,-1.,-1.22464679914735E-16));
#6985=DIRECTION('',(0.,1.22464679914735E-16,-1.));
#6986=DIRECTION('',(0.,-1.,-1.22464679914735E-16));
#6987=DIRECTION('center_axis',(0.5,0.866025403784439,1.06057523872491E-16));
#6988=DIRECTION('ref_axis',(0.866025403784439,-0.5,-6.12323399573677E-17));
#6989=DIRECTION('',(0.866025403784439,-0.5,-6.12323399573677E-17));
#6990=DIRECTION('',(0.,1.22464679914735E-16,-1.));
#6991=DIRECTION('',(0.866025403784439,-0.5,-6.12323399573677E-17));
#6992=DIRECTION('center_axis',(-0.5,0.866025403784439,1.06057523872491E-16));
#6993=DIRECTION('ref_axis',(0.866025403784439,0.5,6.12323399573676E-17));
#6994=DIRECTION('',(0.866025403784439,0.5,6.12323399573676E-17));
#6995=DIRECTION('',(0.,1.22464679914735E-16,-1.));
#6996=DIRECTION('',(0.866025403784439,0.5,6.12323399573676E-17));
#6997=DIRECTION('center_axis',(-1.,6.40987562127855E-16,7.84983366253143E-32));
#6998=DIRECTION('ref_axis',(6.40987562127855E-16,1.,1.22464679914735E-16));
#6999=DIRECTION('',(6.40987562127855E-16,1.,1.22464679914735E-16));
#7000=DIRECTION('',(6.40987562127855E-16,1.,1.22464679914735E-16));
#7001=DIRECTION('center_axis',(0.,1.22464679914735E-16,-1.));
#7002=DIRECTION('ref_axis',(1.,0.,0.));
#7003=DIRECTION('center_axis',(0.,1.22464679914735E-16,-1.));
#7004=DIRECTION('ref_axis',(1.,0.,0.));
#7005=DIRECTION('center_axis',(0.,1.22464679914735E-16,-1.));
#7006=DIRECTION('ref_axis',(1.,0.,0.));
#7007=DIRECTION('',(-0.707106781186547,2.11959791839945E-32,-0.707106781186548));
#7008=DIRECTION('center_axis',(0.,-1.22464679914735E-16,1.));
#7009=DIRECTION('ref_axis',(1.,0.,0.));
#9109=CARTESIAN_POINT('',(0.,0.,0.));
#9110=CARTESIAN_POINT('Origin',(-4.88927830720691,25.1107216927931,9.2));
#9111=CARTESIAN_POINT('',(-7.48735451856023,25.1107216927931,7.7));
#9112=CARTESIAN_POINT('Origin',(-4.88927830720691,25.1107216927931,7.7));
#9113=CARTESIAN_POINT('',(-4.88927830720691,25.1107216927931,6.2));
#9114=CARTESIAN_POINT('Origin',(-4.88927830720691,25.1107216927931,9.2));
#9115=CARTESIAN_POINT('Origin',(-4.88927830720691,25.1107216927931,8.2));
#9116=CARTESIAN_POINT('',(-7.54689383586007,25.1107216927931,7.7));
#9117=CARTESIAN_POINT('Origin',(-4.88927830720691,25.1107216927931,7.7));
#9118=CARTESIAN_POINT('',(-8.04689383586007,25.1107216927931,8.2));
#9119=CARTESIAN_POINT('Origin',(-7.54689383586007,25.1107216927931,8.2));
#9120=CARTESIAN_POINT('Origin',(-4.88927830720691,25.1107216927931,8.2));
#9121=CARTESIAN_POINT('Origin',(-4.88927830720691,25.1107216927931,19.));
#9122=CARTESIAN_POINT('',(-8.04689383586007,25.1107216927931,18.5));
#9123=CARTESIAN_POINT('',(-8.04689383586007,25.1107216927931,19.));
#9124=CARTESIAN_POINT('Origin',(-4.88927830720691,25.1107216927931,18.5));
#9125=CARTESIAN_POINT('Origin',(-4.88927830720691,25.1107216927931,7.7));
#9126=CARTESIAN_POINT('Origin',(-4.88927830720691,23.3786708852242,19.));
#9127=CARTESIAN_POINT('',(-4.88927830720691,23.3786708852242,19.));
#9128=CARTESIAN_POINT('',(-6.38927830720691,24.2446962890086,19.));
#9129=CARTESIAN_POINT('',(-5.26427830720691,23.5951772361703,19.));
#9130=CARTESIAN_POINT('',(-4.88927830720691,23.3786708852242,18.));
#9131=CARTESIAN_POINT('',(-4.88927830720691,23.3786708852242,19.));
#9132=CARTESIAN_POINT('',(-6.38927830720691,24.2446962890086,18.));
#9133=CARTESIAN_POINT('',(-6.38927830720691,24.2446962890086,18.));
#9134=CARTESIAN_POINT('',(-6.38927830720691,24.2446962890086,19.));
#9135=CARTESIAN_POINT('Origin',(-3.38927830720691,24.2446962890086,19.));
#9136=CARTESIAN_POINT('',(-3.38927830720691,24.2446962890086,19.));
#9137=CARTESIAN_POINT('',(-3.76427830720691,24.0281899380625,19.));
#9138=CARTESIAN_POINT('',(-3.38927830720691,24.2446962890086,18.));
#9139=CARTESIAN_POINT('',(-3.38927830720691,24.2446962890086,19.));
#9140=CARTESIAN_POINT('',(-4.88927830720691,23.3786708852242,18.));
#9141=CARTESIAN_POINT('Origin',(-3.38927830720691,25.9767470965775,19.));
#9142=CARTESIAN_POINT('',(-3.38927830720691,25.9767470965775,19.));
#9143=CARTESIAN_POINT('',(-3.38927830720691,25.5437343946853,19.));
#9144=CARTESIAN_POINT('',(-3.38927830720691,25.9767470965775,18.));
#9145=CARTESIAN_POINT('',(-3.38927830720691,25.9767470965775,19.));
#9146=CARTESIAN_POINT('',(-3.38927830720691,24.2446962890086,18.));
#9147=CARTESIAN_POINT('Origin',(-4.88927830720691,26.842772500362,19.));
#9148=CARTESIAN_POINT('',(-4.88927830720691,26.842772500362,19.));
#9149=CARTESIAN_POINT('',(-4.51427830720691,26.6262661494159,19.));
#9150=CARTESIAN_POINT('',(-4.88927830720691,26.842772500362,18.));
#9151=CARTESIAN_POINT('',(-4.88927830720691,26.842772500362,19.));
#9152=CARTESIAN_POINT('',(-3.38927830720691,25.9767470965775,18.));
#9153=CARTESIAN_POINT('Origin',(-6.38927830720691,25.9767470965775,19.));
#9154=CARTESIAN_POINT('',(-6.38927830720691,25.9767470965775,19.));
#9155=CARTESIAN_POINT('',(-6.01427830720691,26.1932534475236,19.));
#9156=CARTESIAN_POINT('',(-6.38927830720691,25.9767470965775,18.));
#9157=CARTESIAN_POINT('',(-6.38927830720691,25.9767470965775,19.));
#9158=CARTESIAN_POINT('',(-4.88927830720691,26.842772500362,18.));
#9159=CARTESIAN_POINT('Origin',(-6.38927830720691,24.2446962890086,19.));
#9160=CARTESIAN_POINT('',(-6.38927830720691,24.6777089909009,19.));
#9161=CARTESIAN_POINT('',(-6.38927830720691,25.9767470965775,18.));
#9162=CARTESIAN_POINT('Origin',(-4.88927830720691,25.1107216927931,18.));
#9163=CARTESIAN_POINT('Origin',(-4.88927830720691,25.1107216927931,18.75));
#9164=CARTESIAN_POINT('',(-7.54689383586007,25.1107216927931,19.));
#9165=CARTESIAN_POINT('Origin',(-4.88927830720691,25.1107216927931,19.));
#9166=CARTESIAN_POINT('',(-7.79689383586007,25.1107216927931,18.75));
#9167=CARTESIAN_POINT('Origin',(-4.88927830720691,25.1107216927931,19.));
#11360=UNCERTAINTY_MEASURE_WITH_UNIT(LENGTH_MEASURE(0.01),#11386,
'DISTANCE_ACCURACY_VALUE',
'Maximum model space distance between geometric entities at asserted c
onnectivities');
#11370=UNCERTAINTY_MEASURE_WITH_UNIT(LENGTH_MEASURE(0.01),#11386,
'DISTANCE_ACCURACY_VALUE',
'Maximum model space distance between geometric entities at asserted c
onnectivities');
#11375=(
GEOMETRIC_REPRESENTATION_CONTEXT(3)
GLOBAL_UNCERTAINTY_ASSIGNED_CONTEXT((#11360))
GLOBAL_UNIT_ASSIGNED_CONTEXT((#11386,#11388,#11389))
REPRESENTATION_CONTEXT('','3D')
);
#11385=(
GEOMETRIC_REPRESENTATION_CONTEXT(3)
GLOBAL_UNCERTAINTY_ASSIGNED_CONTEXT((#11370))
GLOBAL_UNIT_ASSIGNED_CONTEXT((#11386,#11388,#11389))
REPRESENTATION_CONTEXT('','3D')
);
#11386=(
LENGTH_UNIT()
NAMED_UNIT(*)
SI_UNIT(.MILLI.,.METRE.)
);
#11388=(
NAMED_UNIT(*)
PLANE_ANGLE_UNIT()
SI_UNIT($,.RADIAN.)
);
#11389=(
NAMED_UNIT(*)
SI_UNIT($,.STERADIAN.)
SOLID_ANGLE_UNIT()
);
#11394=SHAPE_DEFINITION_REPRESENTATION(#11408,#11435);
#11408=PRODUCT_DEFINITION_SHAPE('',$,#11450);
#11435=SHAPE_REPRESENTATION('',(#5796),#11375);
#11445=PRODUCT_DEFINITION_CONTEXT('part definition',#11489,'design');
#11450=PRODUCT_DEFINITION('Ball_Screw_01','Ball_Screw_01',#11464,#11445);
#11464=PRODUCT_DEFINITION_FORMATION('',$,#11495);
#11489=APPLICATION_CONTEXT(
'Core Data for Automotive Mechanical Design Process');
#11490=PRODUCT_CONTEXT('part definition',#11489,'mechanical');
#11495=PRODUCT('Ball_Screw_01','Ball_Screw_01',$,(#11490));
#11568=COLOUR_RGB('Black',0.12,0.14,0.17);
#11569=FILL_AREA_STYLE_COLOUR('',#11568);
#11570=FILL_AREA_STYLE('',(#11569));
#11571=SURFACE_STYLE_FILL_AREA(#11570);
#11572=SURFACE_SIDE_STYLE('',(#11571));
#11573=SURFACE_STYLE_USAGE(.BOTH.,#11572);
#11574=PRESENTATION_STYLE_ASSIGNMENT((#11573));
ENDSEC;
END-ISO-10303-21;
